ISO-10303-21;
HEADER;
/* Generated by software containing ST-Developer
 * from STEP Tools, Inc. (www.steptools.com) 
 */

FILE_DESCRIPTION(
/* description */ ('PAT-091'),
/* implementation_level */ '2;1');

FILE_NAME(
/* name */ 'Centre bearing retainer (3).step',
/* time_stamp */ '2026-10-27T15:34:44-07:00',
/* author */ (''),
/* organization */ (''),
/* preprocessor_version */ 'ST-DEVELOPER v20.2',
/* originating_system */ 'Autodesk Translation Framework v15.17.0.0',
/* authorisation */ '');

FILE_SCHEMA (('AUTOMOTIVE_DESIGN { 1 0 10303 214 3 1 1 }'));
ENDSEC;

DATA;
#10=MECHANICAL_DESIGN_GEOMETRIC_PRESENTATION_REPRESENTATION('',(#1065),#25100);
#845=SHAPE_REPRESENTATION_RELATIONSHIP('SRR','None',#25612,#955);
#955=ADVANCED_BREP_SHAPE_REPRESENTATION('',(#1186),#25082);
#1065=STYLED_ITEM('',(#26191),#1186);
#1186=MANIFOLD_SOLID_BREP('Body1',#13345);
#1603=FACE_BOUND('',#3960,.T.);
#1604=FACE_BOUND('',#3961,.T.);
#1605=FACE_BOUND('',#3962,.T.);
#1606=FACE_BOUND('',#3963,.T.);
#1607=FACE_BOUND('',#3964,.T.);
#1608=FACE_BOUND('',#3966,.T.);
#1609=FACE_BOUND('',#3967,.T.);
#1610=FACE_BOUND('',#3968,.T.);
#1611=FACE_BOUND('',#3969,.T.);
#1612=FACE_BOUND('',#3970,.T.);
#2010=PLANE('',#16090);
#2011=PLANE('',#16091);
#2747=FACE_OUTER_BOUND('',#3953,.T.);
#2748=FACE_OUTER_BOUND('',#3954,.T.);
#2749=FACE_OUTER_BOUND('',#3955,.T.);
#2750=FACE_OUTER_BOUND('',#3956,.T.);
#2751=FACE_OUTER_BOUND('',#3957,.T.);
#2752=FACE_OUTER_BOUND('',#3958,.T.);
#2753=FACE_OUTER_BOUND('',#3959,.T.);
#2754=FACE_OUTER_BOUND('',#3965,.T.);
#3953=EDGE_LOOP('',(#11624,#11625,#11626,#11627));
#3954=EDGE_LOOP('',(#11628,#11629,#11630,#11631));
#3955=EDGE_LOOP('',(#11632,#11633,#11634,#11635));
#3956=EDGE_LOOP('',(#11636,#11637,#11638,#11639));
#3957=EDGE_LOOP('',(#11640,#11641,#11642,#11643));
#3958=EDGE_LOOP('',(#11644,#11645,#11646,#11647));
#3959=EDGE_LOOP('',(#11648));
#3960=EDGE_LOOP('',(#11649));
#3961=EDGE_LOOP('',(#11650));
#3962=EDGE_LOOP('',(#11651));
#3963=EDGE_LOOP('',(#11652));
#3964=EDGE_LOOP('',(#11653));
#3965=EDGE_LOOP('',(#11654));
#3966=EDGE_LOOP('',(#11655));
#3967=EDGE_LOOP('',(#11656));
#3968=EDGE_LOOP('',(#11657));
#3969=EDGE_LOOP('',(#11658));
#3970=EDGE_LOOP('',(#11659));
#4820=LINE('',#24097,#5560);
#4821=LINE('',#24103,#5561);
#4822=LINE('',#24109,#5562);
#4823=LINE('',#24115,#5563);
#4824=LINE('',#24121,#5564);
#4825=LINE('',#24127,#5565);
#5560=VECTOR('',#20142,0.225000000000001);
#5561=VECTOR('',#20149,0.225000000000001);
#5562=VECTOR('',#20156,0.225000000000001);
#5563=VECTOR('',#20163,0.225000000000001);
#5564=VECTOR('',#20170,1.02);
#5565=VECTOR('',#20177,2.2);
#6230=CIRCLE('',#16073,0.225000000000001);
#6231=CIRCLE('',#16074,0.225000000000001);
#6232=CIRCLE('',#16076,0.225000000000001);
#6233=CIRCLE('',#16077,0.225000000000001);
#6234=CIRCLE('',#16079,0.225000000000001);
#6235=CIRCLE('',#16080,0.225000000000001);
#6236=CIRCLE('',#16082,0.225000000000001);
#6237=CIRCLE('',#16083,0.225000000000001);
#6238=CIRCLE('',#16085,1.02);
#6239=CIRCLE('',#16086,1.02);
#6240=CIRCLE('',#16088,2.2);
#6241=CIRCLE('',#16089,2.2);
#7263=VERTEX_POINT('',#24094);
#7264=VERTEX_POINT('',#24096);
#7265=VERTEX_POINT('',#24100);
#7266=VERTEX_POINT('',#24102);
#7267=VERTEX_POINT('',#24106);
#7268=VERTEX_POINT('',#24108);
#7269=VERTEX_POINT('',#24112);
#7270=VERTEX_POINT('',#24114);
#7271=VERTEX_POINT('',#24118);
#7272=VERTEX_POINT('',#24120);
#7273=VERTEX_POINT('',#24124);
#7274=VERTEX_POINT('',#24126);
#8747=EDGE_CURVE('',#7263,#7263,#6230,.T.);
#8748=EDGE_CURVE('',#7263,#7264,#4820,.T.);
#8749=EDGE_CURVE('',#7264,#7264,#6231,.T.);
#8750=EDGE_CURVE('',#7265,#7265,#6232,.T.);
#8751=EDGE_CURVE('',#7265,#7266,#4821,.T.);
#8752=EDGE_CURVE('',#7266,#7266,#6233,.T.);
#8753=EDGE_CURVE('',#7267,#7267,#6234,.T.);
#8754=EDGE_CURVE('',#7267,#7268,#4822,.T.);
#8755=EDGE_CURVE('',#7268,#7268,#6235,.T.);
#8756=EDGE_CURVE('',#7269,#7269,#6236,.T.);
#8757=EDGE_CURVE('',#7269,#7270,#4823,.T.);
#8758=EDGE_CURVE('',#7270,#7270,#6237,.T.);
#8759=EDGE_CURVE('',#7271,#7271,#6238,.T.);
#8760=EDGE_CURVE('',#7271,#7272,#4824,.T.);
#8761=EDGE_CURVE('',#7272,#7272,#6239,.T.);
#8762=EDGE_CURVE('',#7273,#7273,#6240,.T.);
#8763=EDGE_CURVE('',#7273,#7274,#4825,.T.);
#8764=EDGE_CURVE('',#7274,#7274,#6241,.T.);
#11624=ORIENTED_EDGE('',*,*,#8747,.F.);
#11625=ORIENTED_EDGE('',*,*,#8748,.T.);
#11626=ORIENTED_EDGE('',*,*,#8749,.F.);
#11627=ORIENTED_EDGE('',*,*,#8748,.F.);
#11628=ORIENTED_EDGE('',*,*,#8750,.F.);
#11629=ORIENTED_EDGE('',*,*,#8751,.T.);
#11630=ORIENTED_EDGE('',*,*,#8752,.F.);
#11631=ORIENTED_EDGE('',*,*,#8751,.F.);
#11632=ORIENTED_EDGE('',*,*,#8753,.F.);
#11633=ORIENTED_EDGE('',*,*,#8754,.T.);
#11634=ORIENTED_EDGE('',*,*,#8755,.F.);
#11635=ORIENTED_EDGE('',*,*,#8754,.F.);
#11636=ORIENTED_EDGE('',*,*,#8756,.F.);
#11637=ORIENTED_EDGE('',*,*,#8757,.T.);
#11638=ORIENTED_EDGE('',*,*,#8758,.F.);
#11639=ORIENTED_EDGE('',*,*,#8757,.F.);
#11640=ORIENTED_EDGE('',*,*,#8759,.F.);
#11641=ORIENTED_EDGE('',*,*,#8760,.T.);
#11642=ORIENTED_EDGE('',*,*,#8761,.T.);
#11643=ORIENTED_EDGE('',*,*,#8760,.F.);
#11644=ORIENTED_EDGE('',*,*,#8762,.F.);
#11645=ORIENTED_EDGE('',*,*,#8763,.T.);
#11646=ORIENTED_EDGE('',*,*,#8764,.T.);
#11647=ORIENTED_EDGE('',*,*,#8763,.F.);
#11648=ORIENTED_EDGE('',*,*,#8762,.T.);
#11649=ORIENTED_EDGE('',*,*,#8759,.T.);
#11650=ORIENTED_EDGE('',*,*,#8758,.T.);
#11651=ORIENTED_EDGE('',*,*,#8755,.T.);
#11652=ORIENTED_EDGE('',*,*,#8752,.T.);
#11653=ORIENTED_EDGE('',*,*,#8749,.T.);
#11654=ORIENTED_EDGE('',*,*,#8764,.F.);
#11655=ORIENTED_EDGE('',*,*,#8761,.F.);
#11656=ORIENTED_EDGE('',*,*,#8756,.T.);
#11657=ORIENTED_EDGE('',*,*,#8753,.T.);
#11658=ORIENTED_EDGE('',*,*,#8750,.T.);
#11659=ORIENTED_EDGE('',*,*,#8747,.T.);
#12376=CYLINDRICAL_SURFACE('',#16072,0.225000000000001);
#12377=CYLINDRICAL_SURFACE('',#16075,0.225000000000001);
#12378=CYLINDRICAL_SURFACE('',#16078,0.225000000000001);
#12379=CYLINDRICAL_SURFACE('',#16081,0.225000000000001);
#12380=CYLINDRICAL_SURFACE('',#16084,1.02);
#12381=CYLINDRICAL_SURFACE('',#16087,2.2);
#13114=ADVANCED_FACE('',(#2747),#12376,.F.);
#13115=ADVANCED_FACE('',(#2748),#12377,.F.);
#13116=ADVANCED_FACE('',(#2749),#12378,.F.);
#13117=ADVANCED_FACE('',(#2750),#12379,.F.);
#13118=ADVANCED_FACE('',(#2751),#12380,.F.);
#13119=ADVANCED_FACE('',(#2752),#12381,.T.);
#13120=ADVANCED_FACE('',(#2753,#1603,#1604,#1605,#1606,#1607),#2010,.T.);
#13121=ADVANCED_FACE('',(#2754,#1608,#1609,#1610,#1611,#1612),#2011,.F.);
#13345=CLOSED_SHELL('',(#13114,#13115,#13116,#13117,#13118,#13119,#13120,
#13121));
#16071=AXIS2_PLACEMENT_3D('',#24092,#20136,#20137);
#16072=AXIS2_PLACEMENT_3D('',#24093,#20138,#20139);
#16073=AXIS2_PLACEMENT_3D('',#24095,#20140,#20141);
#16074=AXIS2_PLACEMENT_3D('',#24098,#20143,#20144);
#16075=AXIS2_PLACEMENT_3D('',#24099,#20145,#20146);
#16076=AXIS2_PLACEMENT_3D('',#24101,#20147,#20148);
#16077=AXIS2_PLACEMENT_3D('',#24104,#20150,#20151);
#16078=AXIS2_PLACEMENT_3D('',#24105,#20152,#20153);
#16079=AXIS2_PLACEMENT_3D('',#24107,#20154,#20155);
#16080=AXIS2_PLACEMENT_3D('',#24110,#20157,#20158);
#16081=AXIS2_PLACEMENT_3D('',#24111,#20159,#20160);
#16082=AXIS2_PLACEMENT_3D('',#24113,#20161,#20162);
#16083=AXIS2_PLACEMENT_3D('',#24116,#20164,#20165);
#16084=AXIS2_PLACEMENT_3D('',#24117,#20166,#20167);
#16085=AXIS2_PLACEMENT_3D('',#24119,#20168,#20169);
#16086=AXIS2_PLACEMENT_3D('',#24122,#20171,#20172);
#16087=AXIS2_PLACEMENT_3D('',#24123,#20173,#20174);
#16088=AXIS2_PLACEMENT_3D('',#24125,#20175,#20176);
#16089=AXIS2_PLACEMENT_3D('',#24128,#20178,#20179);
#16090=AXIS2_PLACEMENT_3D('',#24129,#20180,#20181);
#16091=AXIS2_PLACEMENT_3D('',#24130,#20182,#20183);
#20136=DIRECTION('axis',(0.,0.,1.));
#20137=DIRECTION('refdir',(1.,0.,0.));
#20138=DIRECTION('center_axis',(0.,1.,0.));
#20139=DIRECTION('ref_axis',(1.,0.,0.));
#20140=DIRECTION('center_axis',(0.,1.,0.));
#20141=DIRECTION('ref_axis',(1.,0.,0.));
#20142=DIRECTION('',(0.,1.,0.));
#20143=DIRECTION('center_axis',(0.,-1.,0.));
#20144=DIRECTION('ref_axis',(1.,0.,0.));
#20145=DIRECTION('center_axis',(0.,1.,0.));
#20146=DIRECTION('ref_axis',(1.,0.,0.));
#20147=DIRECTION('center_axis',(0.,1.,0.));
#20148=DIRECTION('ref_axis',(1.,0.,0.));
#20149=DIRECTION('',(0.,1.,0.));
#20150=DIRECTION('center_axis',(0.,-1.,0.));
#20151=DIRECTION('ref_axis',(1.,0.,0.));
#20152=DIRECTION('center_axis',(0.,1.,0.));
#20153=DIRECTION('ref_axis',(1.,0.,0.));
#20154=DIRECTION('center_axis',(0.,1.,0.));
#20155=DIRECTION('ref_axis',(1.,0.,0.));
#20156=DIRECTION('',(0.,1.,0.));
#20157=DIRECTION('center_axis',(0.,-1.,0.));
#20158=DIRECTION('ref_axis',(1.,0.,0.));
#20159=DIRECTION('center_axis',(0.,1.,0.));
#20160=DIRECTION('ref_axis',(1.,0.,0.));
#20161=DIRECTION('center_axis',(0.,1.,0.));
#20162=DIRECTION('ref_axis',(1.,0.,0.));
#20163=DIRECTION('',(0.,1.,0.));
#20164=DIRECTION('center_axis',(0.,-1.,0.));
#20165=DIRECTION('ref_axis',(1.,0.,0.));
#20166=DIRECTION('center_axis',(0.,1.,0.));
#20167=DIRECTION('ref_axis',(1.,0.,0.));
#20168=DIRECTION('center_axis',(0.,-1.,0.));
#20169=DIRECTION('ref_axis',(1.,0.,0.));
#20170=DIRECTION('',(0.,-1.,0.));
#20171=DIRECTION('center_axis',(0.,-1.,0.));
#20172=DIRECTION('ref_axis',(1.,0.,0.));
#20173=DIRECTION('center_axis',(0.,1.,0.));
#20174=DIRECTION('ref_axis',(1.,0.,0.));
#20175=DIRECTION('center_axis',(0.,1.,0.));
#20176=DIRECTION('ref_axis',(1.,0.,0.));
#20177=DIRECTION('',(0.,-1.,0.));
#20178=DIRECTION('center_axis',(0.,1.,0.));
#20179=DIRECTION('ref_axis',(1.,0.,0.));
#20180=DIRECTION('center_axis',(0.,1.,0.));
#20181=DIRECTION('ref_axis',(1.,0.,0.));
#20182=DIRECTION('center_axis',(0.,1.,0.));
#20183=DIRECTION('ref_axis',(1.,0.,0.));
#24092=CARTESIAN_POINT('',(0.,0.,0.));
#24093=CARTESIAN_POINT('Origin',(18.056769185842,7.9,6.69185245480489));
#24094=CARTESIAN_POINT('',(17.831769185842,8.,6.69185245480489));
#24095=CARTESIAN_POINT('Origin',(18.056769185842,8.,6.69185245480489));
#24096=CARTESIAN_POINT('',(17.831769185842,8.3,6.69185245480489));
#24097=CARTESIAN_POINT('',(17.831769185842,7.9,6.69185245480489));
#24098=CARTESIAN_POINT('Origin',(18.056769185842,8.3,6.69185245480489));
#24099=CARTESIAN_POINT('Origin',(18.056769185842,7.9,9.30814754519511));
#24100=CARTESIAN_POINT('',(17.831769185842,8.,9.30814754519511));
#24101=CARTESIAN_POINT('Origin',(18.056769185842,8.,9.30814754519511));
#24102=CARTESIAN_POINT('',(17.831769185842,8.3,9.30814754519511));
#24103=CARTESIAN_POINT('',(17.831769185842,7.9,9.30814754519511));
#24104=CARTESIAN_POINT('Origin',(18.056769185842,8.3,9.30814754519511));
#24105=CARTESIAN_POINT('Origin',(20.6730642762322,7.9,9.30814754519511));
#24106=CARTESIAN_POINT('',(20.4480642762322,8.,9.30814754519511));
#24107=CARTESIAN_POINT('Origin',(20.6730642762322,8.,9.30814754519511));
#24108=CARTESIAN_POINT('',(20.4480642762322,8.3,9.30814754519511));
#24109=CARTESIAN_POINT('',(20.4480642762322,7.9,9.30814754519511));
#24110=CARTESIAN_POINT('Origin',(20.6730642762322,8.3,9.30814754519511));
#24111=CARTESIAN_POINT('Origin',(20.6730642762322,7.9,6.69185245480489));
#24112=CARTESIAN_POINT('',(20.4480642762322,8.,6.69185245480489));
#24113=CARTESIAN_POINT('Origin',(20.6730642762322,8.,6.69185245480489));
#24114=CARTESIAN_POINT('',(20.4480642762322,8.3,6.69185245480489));
#24115=CARTESIAN_POINT('',(20.4480642762322,7.9,6.69185245480489));
#24116=CARTESIAN_POINT('Origin',(20.6730642762322,8.3,6.69185245480489));
#24117=CARTESIAN_POINT('Origin',(19.3649167310371,8.,8.));
#24118=CARTESIAN_POINT('',(18.3449167310371,8.3,8.));
#24119=CARTESIAN_POINT('Origin',(19.3649167310371,8.3,8.));
#24120=CARTESIAN_POINT('',(18.3449167310371,8.,8.));
#24121=CARTESIAN_POINT('',(18.3449167310371,8.,8.));
#24122=CARTESIAN_POINT('Origin',(19.3649167310371,8.,8.));
#24123=CARTESIAN_POINT('Origin',(19.3649167310371,8.,8.));
#24124=CARTESIAN_POINT('',(17.1649167310371,8.3,8.));
#24125=CARTESIAN_POINT('Origin',(19.3649167310371,8.3,8.));
#24126=CARTESIAN_POINT('',(17.1649167310371,8.,8.));
#24127=CARTESIAN_POINT('',(17.1649167310371,8.,8.));
#24128=CARTESIAN_POINT('Origin',(19.3649167310371,8.,8.));
#24129=CARTESIAN_POINT('Origin',(19.3649167310371,8.3,8.));
#24130=CARTESIAN_POINT('Origin',(19.3649167310371,8.,8.));
#24961=UNCERTAINTY_MEASURE_WITH_UNIT(LENGTH_MEASURE(0.001),#25101,
'DISTANCE_ACCURACY_VALUE',
'Maximum model space distance between geometric entities at asserted c
onnectivities');
#24979=UNCERTAINTY_MEASURE_WITH_UNIT(LENGTH_MEASURE(0.001),#25101,
'DISTANCE_ACCURACY_VALUE',
'Maximum model space distance between geometric entities at asserted c
onnectivities');
#25082=(
GEOMETRIC_REPRESENTATION_CONTEXT(3)
GLOBAL_UNCERTAINTY_ASSIGNED_CONTEXT((#24961))
GLOBAL_UNIT_ASSIGNED_CONTEXT((#25101,#25103,#25104))
REPRESENTATION_CONTEXT('','3D')
);
#25100=(
GEOMETRIC_REPRESENTATION_CONTEXT(3)
GLOBAL_UNCERTAINTY_ASSIGNED_CONTEXT((#24979))
GLOBAL_UNIT_ASSIGNED_CONTEXT((#25101,#25103,#25104))
REPRESENTATION_CONTEXT('','3D')
);
#25101=(
LENGTH_UNIT()
NAMED_UNIT(*)
SI_UNIT(.CENTI.,.METRE.)
);
#25103=(
NAMED_UNIT(*)
PLANE_ANGLE_UNIT()
SI_UNIT($,.RADIAN.)
);
#25104=(
NAMED_UNIT(*)
SI_UNIT($,.STERADIAN.)
SOLID_ANGLE_UNIT()
);
#25207=SHAPE_DEFINITION_REPRESENTATION(#25401,#25612);
#25401=PRODUCT_DEFINITION_SHAPE('',$,#25733);
#25612=SHAPE_REPRESENTATION('',(#16071),#25082);
#25630=PRODUCT_DEFINITION_CONTEXT('part definition',#25992,'design');
#25733=PRODUCT_DEFINITION('Centre bearing retainer (3)',
'Centre bearing retainer (3)',#25853,#25630);
#25853=PRODUCT_DEFINITION_FORMATION('',$,#26096);
#25992=APPLICATION_CONTEXT(
'Core Data for Automotive Mechanical Design Process');
#25993=PRODUCT_CONTEXT('part definition',#25992,'mechanical');
#26096=PRODUCT('Centre bearing retainer (3)',
'Centre bearing retainer (3)','Centre bearing retainer (3)',(#25993));
#26185=COLOUR_RGB('Grey',0.48,0.52,0.57);
#26186=FILL_AREA_STYLE_COLOUR('',#26185);
#26187=FILL_AREA_STYLE('',(#26186));
#26188=SURFACE_STYLE_FILL_AREA(#26187);
#26189=SURFACE_SIDE_STYLE('',(#26188));
#26190=SURFACE_STYLE_USAGE(.BOTH.,#26189);
#26191=PRESENTATION_STYLE_ASSIGNMENT((#26190));
ENDSEC;
END-ISO-10303-21;
